ISO-10303-21;
HEADER;
/* Generated by software containing ST-Developer
 * from STEP Tools, Inc. (www.steptools.com) 
 */

FILE_DESCRIPTION(
/* description */ ('Crank-driven oscillating fan base (mechanism only)'),

/* implementation_level */ '2;1');

FILE_NAME(
/* name */ 'M5x14 Cap Screw.step',
/* time_stamp */ '2026-10-28T03:25:00-07:00',
/* author */ (''),
/* organization */ (''),
/* preprocessor_version */ 'ST-DEVELOPER v20.2',
/* originating_system */ 'Autodesk Translation Framework v15.17.0.0',
/* authorisation */ '');

FILE_SCHEMA (('AUTOMOTIVE_DESIGN { 1 0 10303 214 3 1 1 }'));
ENDSEC;

DATA;
#10=MECHANICAL_DESIGN_GEOMETRIC_PRESENTATION_REPRESENTATION('',(#445),#11916);
#293=CONICAL_SURFACE('',#6818,0.4,0.785398163397448);
#294=CONICAL_SURFACE('',#6822,0.41,0.785398163397448);
#295=CONICAL_SURFACE('',#6826,0.26,0.463647609000806);
#310=ORIENTED_CLOSED_SHELL('',*,#6075,.F.);
#313=BREP_WITH_VOIDS('Body1',#6076,(#310));
#365=SHAPE_REPRESENTATION_RELATIONSHIP('SRR','None',#12089,#405);
#405=ADVANCED_BREP_SHAPE_REPRESENTATION('',(#313),#11880);
#445=STYLED_ITEM('',(#12382),#313);
#606=FACE_BOUND('',#1459,.T.);
#742=PLANE('',#6806);
#743=PLANE('',#6807);
#744=PLANE('',#6808);
#745=PLANE('',#6809);
#746=PLANE('',#6810);
#747=PLANE('',#6811);
#748=PLANE('',#6812);
#749=PLANE('',#6813);
#750=PLANE('',#6814);
#751=PLANE('',#6816);
#752=PLANE('',#6824);
#994=FACE_OUTER_BOUND('',#1445,.T.);
#995=FACE_OUTER_BOUND('',#1446,.T.);
#996=FACE_OUTER_BOUND('',#1447,.T.);
#997=FACE_OUTER_BOUND('',#1448,.T.);
#998=FACE_OUTER_BOUND('',#1449,.T.);
#999=FACE_OUTER_BOUND('',#1450,.T.);
#1000=FACE_OUTER_BOUND('',#1451,.T.);
#1001=FACE_OUTER_BOUND('',#1452,.T.);
#1002=FACE_OUTER_BOUND('',#1453,.T.);
#1003=FACE_OUTER_BOUND('',#1454,.T.);
#1004=FACE_OUTER_BOUND('',#1455,.T.);
#1005=FACE_OUTER_BOUND('',#1456,.T.);
#1006=FACE_OUTER_BOUND('',#1457,.T.);
#1007=FACE_OUTER_BOUND('',#1458,.T.);
#1008=FACE_OUTER_BOUND('',#1460,.T.);
#1009=FACE_OUTER_BOUND('',#1461,.T.);
#1445=EDGE_LOOP('',(#4544,#4545,#4546,#4547));
#1446=EDGE_LOOP('',(#4548,#4549,#4550,#4551));
#1447=EDGE_LOOP('',(#4552,#4553,#4554,#4555));
#1448=EDGE_LOOP('',(#4556,#4557,#4558,#4559));
#1449=EDGE_LOOP('',(#4560,#4561,#4562,#4563));
#1450=EDGE_LOOP('',(#4564,#4565,#4566,#4567));
#1451=EDGE_LOOP('',(#4568,#4569,#4570,#4571,#4572,#4573));
#1452=EDGE_LOOP('',(#4574,#4575,#4576,#4577,#4578,#4579));
#1453=EDGE_LOOP('',(#4580));
#1454=EDGE_LOOP('',(#4581));
#1455=EDGE_LOOP('',(#4582,#4583,#4584,#4585));
#1456=EDGE_LOOP('',(#4586,#4587,#4588,#4589));
#1457=EDGE_LOOP('',(#4590,#4591,#4592,#4593));
#1458=EDGE_LOOP('',(#4594));
#1459=EDGE_LOOP('',(#4595));
#1460=EDGE_LOOP('',(#4596,#4597,#4598,#4599));
#1461=EDGE_LOOP('',(#4600,#4601,#4602,#4603));
#1900=LINE('',#10104,#2233);
#1901=LINE('',#10106,#2234);
#1902=LINE('',#10108,#2235);
#1903=LINE('',#10109,#2236);
#1904=LINE('',#10112,#2237);
#1905=LINE('',#10114,#2238);
#1906=LINE('',#10115,#2239);
#1907=LINE('',#10118,#2240);
#1908=LINE('',#10120,#2241);
#1909=LINE('',#10121,#2242);
#1910=LINE('',#10124,#2243);
#1911=LINE('',#10126,#2244);
#1912=LINE('',#10127,#2245);
#1913=LINE('',#10130,#2246);
#1914=LINE('',#10132,#2247);
#1915=LINE('',#10133,#2248);
#1916=LINE('',#10135,#2249);
#1917=LINE('',#10136,#2250);
#1918=LINE('',#10148,#2251);
#1919=LINE('',#10152,#2252);
#1920=LINE('',#10156,#2253);
#1921=LINE('',#10163,#2254);
#1922=LINE('',#10165,#2255);
#2233=VECTOR('',#8009,1.);
#2234=VECTOR('',#8010,1.);
#2235=VECTOR('',#8011,1.);
#2236=VECTOR('',#8012,1.);
#2237=VECTOR('',#8015,1.);
#2238=VECTOR('',#8016,1.);
#2239=VECTOR('',#8017,1.);
#2240=VECTOR('',#8020,1.);
#2241=VECTOR('',#8021,1.);
#2242=VECTOR('',#8022,1.);
#2243=VECTOR('',#8025,1.);
#2244=VECTOR('',#8026,1.);
#2245=VECTOR('',#8027,1.);
#2246=VECTOR('',#8030,1.);
#2247=VECTOR('',#8031,1.);
#2248=VECTOR('',#8032,1.);
#2249=VECTOR('',#8035,1.);
#2250=VECTOR('',#8036,1.);
#2251=VECTOR('',#8053,0.4);
#2252=VECTOR('',#8058,0.425);
#2253=VECTOR('',#8063,0.41);
#2254=VECTOR('',#8072,0.26);
#2255=VECTOR('',#8075,0.25);
#2592=CIRCLE('',#6815,0.24505);
#2593=CIRCLE('',#6817,0.375);
#2594=CIRCLE('',#6819,0.425);
#2595=CIRCLE('',#6821,0.425);
#2596=CIRCLE('',#6823,0.395);
#2597=CIRCLE('',#6825,0.27);
#2598=CIRCLE('',#6827,0.24505);
#2989=VERTEX_POINT('',#10102);
#2990=VERTEX_POINT('',#10103);
#2991=VERTEX_POINT('',#10105);
#2992=VERTEX_POINT('',#10107);
#2993=VERTEX_POINT('',#10111);
#2994=VERTEX_POINT('',#10113);
#2995=VERTEX_POINT('',#10117);
#2996=VERTEX_POINT('',#10119);
#2997=VERTEX_POINT('',#10123);
#2998=VERTEX_POINT('',#10125);
#2999=VERTEX_POINT('',#10129);
#3000=VERTEX_POINT('',#10131);
#3001=VERTEX_POINT('',#10140);
#3002=VERTEX_POINT('',#10143);
#3003=VERTEX_POINT('',#10146);
#3004=VERTEX_POINT('',#10150);
#3005=VERTEX_POINT('',#10154);
#3006=VERTEX_POINT('',#10158);
#3007=VERTEX_POINT('',#10161);
#3567=EDGE_CURVE('',#2989,#2990,#1900,.T.);
#3568=EDGE_CURVE('',#2990,#2991,#1901,.T.);
#3569=EDGE_CURVE('',#2991,#2992,#1902,.T.);
#3570=EDGE_CURVE('',#2989,#2992,#1903,.T.);
#3571=EDGE_CURVE('',#2990,#2993,#1904,.T.);
#3572=EDGE_CURVE('',#2993,#2994,#1905,.T.);
#3573=EDGE_CURVE('',#2994,#2991,#1906,.T.);
#3574=EDGE_CURVE('',#2993,#2995,#1907,.T.);
#3575=EDGE_CURVE('',#2995,#2996,#1908,.T.);
#3576=EDGE_CURVE('',#2996,#2994,#1909,.T.);
#3577=EDGE_CURVE('',#2995,#2997,#1910,.T.);
#3578=EDGE_CURVE('',#2997,#2998,#1911,.T.);
#3579=EDGE_CURVE('',#2998,#2996,#1912,.T.);
#3580=EDGE_CURVE('',#2997,#2999,#1913,.T.);
#3581=EDGE_CURVE('',#2999,#3000,#1914,.T.);
#3582=EDGE_CURVE('',#3000,#2998,#1915,.T.);
#3583=EDGE_CURVE('',#2999,#2989,#1916,.T.);
#3584=EDGE_CURVE('',#2992,#3000,#1917,.T.);
#3585=EDGE_CURVE('',#3001,#3001,#2592,.T.);
#3586=EDGE_CURVE('',#3002,#3002,#2593,.T.);
#3587=EDGE_CURVE('',#3003,#3003,#2594,.T.);
#3588=EDGE_CURVE('',#3003,#3002,#1918,.T.);
#3589=EDGE_CURVE('',#3004,#3004,#2595,.T.);
#3590=EDGE_CURVE('',#3004,#3003,#1919,.T.);
#3591=EDGE_CURVE('',#3005,#3005,#2596,.T.);
#3592=EDGE_CURVE('',#3005,#3004,#1920,.T.);
#3593=EDGE_CURVE('',#3006,#3006,#2597,.T.);
#3594=EDGE_CURVE('',#3007,#3007,#2598,.F.);
#3595=EDGE_CURVE('',#3007,#3006,#1921,.T.);
#3596=EDGE_CURVE('',#3001,#3007,#1922,.T.);
#4544=ORIENTED_EDGE('',*,*,#3567,.T.);
#4545=ORIENTED_EDGE('',*,*,#3568,.T.);
#4546=ORIENTED_EDGE('',*,*,#3569,.T.);
#4547=ORIENTED_EDGE('',*,*,#3570,.F.);
#4548=ORIENTED_EDGE('',*,*,#3571,.T.);
#4549=ORIENTED_EDGE('',*,*,#3572,.T.);
#4550=ORIENTED_EDGE('',*,*,#3573,.T.);
#4551=ORIENTED_EDGE('',*,*,#3568,.F.);
#4552=ORIENTED_EDGE('',*,*,#3574,.T.);
#4553=ORIENTED_EDGE('',*,*,#3575,.T.);
#4554=ORIENTED_EDGE('',*,*,#3576,.T.);
#4555=ORIENTED_EDGE('',*,*,#3572,.F.);
#4556=ORIENTED_EDGE('',*,*,#3577,.T.);
#4557=ORIENTED_EDGE('',*,*,#3578,.T.);
#4558=ORIENTED_EDGE('',*,*,#3579,.T.);
#4559=ORIENTED_EDGE('',*,*,#3575,.F.);
#4560=ORIENTED_EDGE('',*,*,#3580,.T.);
#4561=ORIENTED_EDGE('',*,*,#3581,.T.);
#4562=ORIENTED_EDGE('',*,*,#3582,.T.);
#4563=ORIENTED_EDGE('',*,*,#3578,.F.);
#4564=ORIENTED_EDGE('',*,*,#3583,.T.);
#4565=ORIENTED_EDGE('',*,*,#3570,.T.);
#4566=ORIENTED_EDGE('',*,*,#3584,.T.);
#4567=ORIENTED_EDGE('',*,*,#3581,.F.);
#4568=ORIENTED_EDGE('',*,*,#3583,.F.);
#4569=ORIENTED_EDGE('',*,*,#3580,.F.);
#4570=ORIENTED_EDGE('',*,*,#3577,.F.);
#4571=ORIENTED_EDGE('',*,*,#3574,.F.);
#4572=ORIENTED_EDGE('',*,*,#3571,.F.);
#4573=ORIENTED_EDGE('',*,*,#3567,.F.);
#4574=ORIENTED_EDGE('',*,*,#3584,.F.);
#4575=ORIENTED_EDGE('',*,*,#3569,.F.);
#4576=ORIENTED_EDGE('',*,*,#3573,.F.);
#4577=ORIENTED_EDGE('',*,*,#3576,.F.);
#4578=ORIENTED_EDGE('',*,*,#3579,.F.);
#4579=ORIENTED_EDGE('',*,*,#3582,.F.);
#4580=ORIENTED_EDGE('',*,*,#3585,.F.);
#4581=ORIENTED_EDGE('',*,*,#3586,.F.);
#4582=ORIENTED_EDGE('',*,*,#3587,.F.);
#4583=ORIENTED_EDGE('',*,*,#3588,.T.);
#4584=ORIENTED_EDGE('',*,*,#3586,.T.);
#4585=ORIENTED_EDGE('',*,*,#3588,.F.);
#4586=ORIENTED_EDGE('',*,*,#3589,.F.);
#4587=ORIENTED_EDGE('',*,*,#3590,.T.);
#4588=ORIENTED_EDGE('',*,*,#3587,.T.);
#4589=ORIENTED_EDGE('',*,*,#3590,.F.);
#4590=ORIENTED_EDGE('',*,*,#3591,.F.);
#4591=ORIENTED_EDGE('',*,*,#3592,.T.);
#4592=ORIENTED_EDGE('',*,*,#3589,.T.);
#4593=ORIENTED_EDGE('',*,*,#3592,.F.);
#4594=ORIENTED_EDGE('',*,*,#3591,.T.);
#4595=ORIENTED_EDGE('',*,*,#3593,.F.);
#4596=ORIENTED_EDGE('',*,*,#3594,.F.);
#4597=ORIENTED_EDGE('',*,*,#3595,.T.);
#4598=ORIENTED_EDGE('',*,*,#3593,.T.);
#4599=ORIENTED_EDGE('',*,*,#3595,.F.);
#4600=ORIENTED_EDGE('',*,*,#3585,.T.);
#4601=ORIENTED_EDGE('',*,*,#3596,.T.);
#4602=ORIENTED_EDGE('',*,*,#3594,.T.);
#4603=ORIENTED_EDGE('',*,*,#3596,.F.);
#5604=CYLINDRICAL_SURFACE('',#6820,0.425);
#5605=CYLINDRICAL_SURFACE('',#6828,0.24505);
#5800=ADVANCED_FACE('',(#994),#742,.F.);
#5801=ADVANCED_FACE('',(#995),#743,.F.);
#5802=ADVANCED_FACE('',(#996),#744,.F.);
#5803=ADVANCED_FACE('',(#997),#745,.F.);
#5804=ADVANCED_FACE('',(#998),#746,.F.);
#5805=ADVANCED_FACE('',(#999),#747,.F.);
#5806=ADVANCED_FACE('',(#1000),#748,.F.);
#5807=ADVANCED_FACE('',(#1001),#749,.F.);
#5808=ADVANCED_FACE('',(#1002),#750,.F.);
#5809=ADVANCED_FACE('',(#1003),#751,.T.);
#5810=ADVANCED_FACE('',(#1004),#293,.T.);
#5811=ADVANCED_FACE('',(#1005),#5604,.T.);
#5812=ADVANCED_FACE('',(#1006),#294,.T.);
#5813=ADVANCED_FACE('',(#1007,#606),#752,.T.);
#5814=ADVANCED_FACE('',(#1008),#295,.T.);
#5815=ADVANCED_FACE('',(#1009),#5605,.T.);
#6075=CLOSED_SHELL('',(#5800,#5801,#5802,#5803,#5804,#5805,#5806,#5807));
#6076=CLOSED_SHELL('',(#5808,#5809,#5810,#5811,#5812,#5813,#5814,#5815));
#6805=AXIS2_PLACEMENT_3D('',#10100,#8005,#8006);
#6806=AXIS2_PLACEMENT_3D('',#10101,#8007,#8008);
#6807=AXIS2_PLACEMENT_3D('',#10110,#8013,#8014);
#6808=AXIS2_PLACEMENT_3D('',#10116,#8018,#8019);
#6809=AXIS2_PLACEMENT_3D('',#10122,#8023,#8024);
#6810=AXIS2_PLACEMENT_3D('',#10128,#8028,#8029);
#6811=AXIS2_PLACEMENT_3D('',#10134,#8033,#8034);
#6812=AXIS2_PLACEMENT_3D('',#10137,#8037,#8038);
#6813=AXIS2_PLACEMENT_3D('',#10138,#8039,#8040);
#6814=AXIS2_PLACEMENT_3D('',#10139,#8041,#8042);
#6815=AXIS2_PLACEMENT_3D('',#10141,#8043,#8044);
#6816=AXIS2_PLACEMENT_3D('',#10142,#8045,#8046);
#6817=AXIS2_PLACEMENT_3D('',#10144,#8047,#8048);
#6818=AXIS2_PLACEMENT_3D('',#10145,#8049,#8050);
#6819=AXIS2_PLACEMENT_3D('',#10147,#8051,#8052);
#6820=AXIS2_PLACEMENT_3D('',#10149,#8054,#8055);
#6821=AXIS2_PLACEMENT_3D('',#10151,#8056,#8057);
#6822=AXIS2_PLACEMENT_3D('',#10153,#8059,#8060);
#6823=AXIS2_PLACEMENT_3D('',#10155,#8061,#8062);
#6824=AXIS2_PLACEMENT_3D('',#10157,#8064,#8065);
#6825=AXIS2_PLACEMENT_3D('',#10159,#8066,#8067);
#6826=AXIS2_PLACEMENT_3D('',#10160,#8068,#8069);
#6827=AXIS2_PLACEMENT_3D('',#10162,#8070,#8071);
#6828=AXIS2_PLACEMENT_3D('',#10164,#8073,#8074);
#8005=DIRECTION('axis',(0.,0.,1.));
#8006=DIRECTION('refdir',(1.,0.,0.));
#8007=DIRECTION('center_axis',(0.866025403784439,0.,-0.5));
#8008=DIRECTION('ref_axis',(0.5,0.,0.866025403784439));
#8009=DIRECTION('',(-0.5,0.,-0.866025403784439));
#8010=DIRECTION('',(0.,-1.,0.));
#8011=DIRECTION('',(0.5,0.,0.866025403784439));
#8012=DIRECTION('',(0.,-1.,0.));
#8013=DIRECTION('center_axis',(1.20185167898973E-16,0.,-1.));
#8014=DIRECTION('ref_axis',(1.,0.,1.20185167898973E-16));
#8015=DIRECTION('',(-1.,0.,-1.20185167898973E-16));
#8016=DIRECTION('',(0.,-1.,0.));
#8017=DIRECTION('',(1.,0.,1.20185167898973E-16));
#8018=DIRECTION('center_axis',(-0.866025403784439,0.,-0.5));
#8019=DIRECTION('ref_axis',(0.5,0.,-0.866025403784439));
#8020=DIRECTION('',(-0.5,0.,0.866025403784439));
#8021=DIRECTION('',(0.,-1.,0.));
#8022=DIRECTION('',(0.5,0.,-0.866025403784439));
#8023=DIRECTION('center_axis',(-0.866025403784439,0.,0.5));
#8024=DIRECTION('ref_axis',(-0.5,0.,-0.866025403784439));
#8025=DIRECTION('',(0.5,0.,0.866025403784439));
#8026=DIRECTION('',(0.,-1.,0.));
#8027=DIRECTION('',(-0.5,0.,-0.866025403784439));
#8028=DIRECTION('center_axis',(-2.40370335797945E-16,0.,1.));
#8029=DIRECTION('ref_axis',(-1.,0.,-2.40370335797945E-16));
#8030=DIRECTION('',(1.,0.,2.40370335797945E-16));
#8031=DIRECTION('',(0.,-1.,0.));
#8032=DIRECTION('',(-1.,0.,-2.40370335797945E-16));
#8033=DIRECTION('center_axis',(0.866025403784439,0.,0.5));
#8034=DIRECTION('ref_axis',(-0.5,0.,0.866025403784439));
#8035=DIRECTION('',(0.5,0.,-0.866025403784439));
#8036=DIRECTION('',(-0.5,0.,0.866025403784439));
#8037=DIRECTION('center_axis',(0.,1.,0.));
#8038=DIRECTION('ref_axis',(1.,0.,0.));
#8039=DIRECTION('center_axis',(0.,-1.,0.));
#8040=DIRECTION('ref_axis',(0.,0.,-1.));
#8041=DIRECTION('center_axis',(0.,1.,0.));
#8042=DIRECTION('ref_axis',(1.,0.,0.));
#8043=DIRECTION('center_axis',(0.,1.,0.));
#8044=DIRECTION('ref_axis',(1.,0.,0.));
#8045=DIRECTION('center_axis',(0.,1.,0.));
#8046=DIRECTION('ref_axis',(0.,0.,1.));
#8047=DIRECTION('center_axis',(0.,-1.,0.));
#8048=DIRECTION('ref_axis',(1.,0.,0.));
#8049=DIRECTION('center_axis',(0.,-1.,0.));
#8050=DIRECTION('ref_axis',(1.,0.,0.));
#8051=DIRECTION('center_axis',(0.,-1.,0.));
#8052=DIRECTION('ref_axis',(1.,0.,0.));
#8053=DIRECTION('',(0.707106781186548,0.707106781186547,8.65956056235493E-17));
#8054=DIRECTION('center_axis',(0.,-1.,0.));
#8055=DIRECTION('ref_axis',(1.,0.,0.));
#8056=DIRECTION('center_axis',(0.,-1.,0.));
#8057=DIRECTION('ref_axis',(1.,0.,0.));
#8058=DIRECTION('',(0.,1.,0.));
#8059=DIRECTION('center_axis',(0.,1.,0.));
#8060=DIRECTION('ref_axis',(1.,0.,0.));
#8061=DIRECTION('center_axis',(0.,-1.,0.));
#8062=DIRECTION('ref_axis',(1.,0.,0.));
#8063=DIRECTION('',(-0.707106781186547,0.707106781186548,-8.65956056235493E-17));
#8064=DIRECTION('center_axis',(0.,-1.,0.));
#8065=DIRECTION('ref_axis',(0.,0.,-1.));
#8066=DIRECTION('center_axis',(0.,-1.,0.));
#8067=DIRECTION('ref_axis',(1.,0.,0.));
#8068=DIRECTION('center_axis',(0.,1.,0.));
#8069=DIRECTION('ref_axis',(1.,0.,0.));
#8070=DIRECTION('center_axis',(0.,1.,0.));
#8071=DIRECTION('ref_axis',(1.,0.,0.));
#8072=DIRECTION('',(-0.447213595499958,0.894427190999916,-5.47678698264203E-17));
#8073=DIRECTION('center_axis',(0.,-1.,0.));
#8074=DIRECTION('ref_axis',(1.,0.,0.));
#8075=DIRECTION('',(0.,1.,0.));
#10100=CARTESIAN_POINT('',(0.,0.,0.));
#10101=CARTESIAN_POINT('Origin',(0.115470053837925,-0.5,-0.2));
#10102=CARTESIAN_POINT('',(0.23094010767585,-0.5,0.));
#10103=CARTESIAN_POINT('',(0.115470053837925,-0.5,-0.2));
#10104=CARTESIAN_POINT('',(0.23094010767585,-0.5,0.));
#10105=CARTESIAN_POINT('',(0.115470053837925,-0.8,-0.2));
#10106=CARTESIAN_POINT('',(0.115470053837925,-0.5,-0.2));
#10107=CARTESIAN_POINT('',(0.23094010767585,-0.8,0.));
#10108=CARTESIAN_POINT('',(0.23094010767585,-0.8,0.));
#10109=CARTESIAN_POINT('',(0.23094010767585,-0.5,0.));
#10110=CARTESIAN_POINT('Origin',(-0.115470053837925,-0.5,-0.2));
#10111=CARTESIAN_POINT('',(-0.115470053837925,-0.5,-0.2));
#10112=CARTESIAN_POINT('',(0.115470053837925,-0.5,-0.2));
#10113=CARTESIAN_POINT('',(-0.115470053837925,-0.8,-0.2));
#10114=CARTESIAN_POINT('',(-0.115470053837925,-0.5,-0.2));
#10115=CARTESIAN_POINT('',(0.115470053837925,-0.8,-0.2));
#10116=CARTESIAN_POINT('Origin',(-0.23094010767585,-0.5,-2.77555756156289E-17));
#10117=CARTESIAN_POINT('',(-0.23094010767585,-0.5,-2.82820063659975E-17));
#10118=CARTESIAN_POINT('',(-0.115470053837925,-0.5,-0.2));
#10119=CARTESIAN_POINT('',(-0.23094010767585,-0.8,-2.77555756156289E-17));
#10120=CARTESIAN_POINT('',(-0.23094010767585,-0.5,-2.82820063659975E-17));
#10121=CARTESIAN_POINT('',(-0.115470053837925,-0.8,-0.2));
#10122=CARTESIAN_POINT('Origin',(-0.115470053837925,-0.5,0.2));
#10123=CARTESIAN_POINT('',(-0.115470053837925,-0.5,0.2));
#10124=CARTESIAN_POINT('',(-0.23094010767585,-0.5,-2.82820063659975E-17));
#10125=CARTESIAN_POINT('',(-0.115470053837925,-0.8,0.2));
#10126=CARTESIAN_POINT('',(-0.115470053837925,-0.5,0.2));
#10127=CARTESIAN_POINT('',(-0.23094010767585,-0.8,-2.82820063659975E-17));
#10128=CARTESIAN_POINT('Origin',(0.115470053837925,-0.5,0.2));
#10129=CARTESIAN_POINT('',(0.115470053837925,-0.5,0.2));
#10130=CARTESIAN_POINT('',(-0.115470053837925,-0.5,0.2));
#10131=CARTESIAN_POINT('',(0.115470053837925,-0.8,0.2));
#10132=CARTESIAN_POINT('',(0.115470053837925,-0.5,0.2));
#10133=CARTESIAN_POINT('',(-0.115470053837925,-0.8,0.2));
#10134=CARTESIAN_POINT('Origin',(0.23094010767585,-0.5,0.));
#10135=CARTESIAN_POINT('',(0.115470053837925,-0.5,0.2));
#10136=CARTESIAN_POINT('',(0.115470053837925,-0.8,0.2));
#10137=CARTESIAN_POINT('Origin',(0.,-0.5,0.));
#10138=CARTESIAN_POINT('Origin',(0.,-0.8,0.));
#10139=CARTESIAN_POINT('Origin',(0.,-1.4,0.));
#10140=CARTESIAN_POINT('',(-0.24505,-1.4,3.00099698131059E-17));
#10141=CARTESIAN_POINT('Origin',(0.,-1.4,0.));
#10142=CARTESIAN_POINT('Origin',(0.375,0.5,0.));
#10143=CARTESIAN_POINT('',(-0.375,0.5,-4.59242549680257E-17));
#10144=CARTESIAN_POINT('Origin',(0.,0.5,0.));
#10145=CARTESIAN_POINT('Origin',(0.,0.475,0.));
#10146=CARTESIAN_POINT('',(-0.425,0.45,-5.20474889637625E-17));
#10147=CARTESIAN_POINT('Origin',(0.,0.45,0.));
#10148=CARTESIAN_POINT('',(-0.4,0.475,-4.89858719658941E-17));
#10149=CARTESIAN_POINT('Origin',(0.,0.24,0.));
#10150=CARTESIAN_POINT('',(-0.425,0.0299999999999998,-5.20474889637625E-17));
#10151=CARTESIAN_POINT('Origin',(0.,0.0299999999999998,0.));
#10152=CARTESIAN_POINT('',(-0.425,0.24,-5.20474889637625E-17));
#10153=CARTESIAN_POINT('Origin',(0.,0.0150000000000001,0.));
#10154=CARTESIAN_POINT('',(-0.395,4.85722573273506E-17,-4.83735485663204E-17));
#10155=CARTESIAN_POINT('Origin',(0.,0.,0.));
#10156=CARTESIAN_POINT('',(-0.41,0.0150000000000001,-5.02105187650415E-17));
#10157=CARTESIAN_POINT('Origin',(0.27,0.,0.));
#10158=CARTESIAN_POINT('',(-0.27,0.,-3.30654635769785E-17));
#10159=CARTESIAN_POINT('Origin',(0.,0.,0.));
#10160=CARTESIAN_POINT('Origin',(0.,-0.02,0.));
#10161=CARTESIAN_POINT('',(-0.24505,-0.0498999999999999,3.00099698131059E-17));
#10162=CARTESIAN_POINT('Origin',(0.,-0.0498999999999999,0.));
#10163=CARTESIAN_POINT('',(-0.26,-0.02,-3.18408167778312E-17));
#10164=CARTESIAN_POINT('Origin',(0.,-0.995,0.));
#10165=CARTESIAN_POINT('',(-0.24505,-0.995,-3.00099698131059E-17));
#11833=UNCERTAINTY_MEASURE_WITH_UNIT(LENGTH_MEASURE(0.001),#11917,
'DISTANCE_ACCURACY_VALUE',
'Maximum model space distance between geometric entities at asserted c
onnectivities');
#11869=UNCERTAINTY_MEASURE_WITH_UNIT(LENGTH_MEASURE(0.001),#11917,
'DISTANCE_ACCURACY_VALUE',
'Maximum model space distance between geometric entities at asserted c
onnectivities');
#11880=(
GEOMETRIC_REPRESENTATION_CONTEXT(3)
GLOBAL_UNCERTAINTY_ASSIGNED_CONTEXT((#11833))
GLOBAL_UNIT_ASSIGNED_CONTEXT((#11917,#11919,#11920))
REPRESENTATION_CONTEXT('','3D')
);
#11916=(
GEOMETRIC_REPRESENTATION_CONTEXT(3)
GLOBAL_UNCERTAINTY_ASSIGNED_CONTEXT((#11869))
GLOBAL_UNIT_ASSIGNED_CONTEXT((#11917,#11919,#11920))
REPRESENTATION_CONTEXT('','3D')
);
#11917=(
LENGTH_UNIT()
NAMED_UNIT(*)
SI_UNIT(.CENTI.,.METRE.)
);
#11919=(
NAMED_UNIT(*)
PLANE_ANGLE_UNIT()
SI_UNIT($,.RADIAN.)
);
#11920=(
NAMED_UNIT(*)
SI_UNIT($,.STERADIAN.)
SOLID_ANGLE_UNIT()
);
#11931=SHAPE_DEFINITION_REPRESENTATION(#11977,#12089);
#11977=PRODUCT_DEFINITION_SHAPE('',$,#12136);
#12089=SHAPE_REPRESENTATION('',(#6805),#11880);
#12125=PRODUCT_DEFINITION_CONTEXT('part definition',#12265,'design');
#12136=PRODUCT_DEFINITION('M5x14 Cap Screw','M5x14 Cap Screw',#12182,#12125);
#12182=PRODUCT_DEFINITION_FORMATION('',$,#12277);
#12265=APPLICATION_CONTEXT(
'Core Data for Automotive Mechanical Design Process');
#12266=PRODUCT_CONTEXT('part definition',#12265,'mechanical');
#12277=PRODUCT('M5x14 Cap Screw','M5x14 Cap Screw','M5x14 Cap Screw',(#12266));
#12376=COLOUR_RGB('Black',0.12,0.14,0.17);
#12377=FILL_AREA_STYLE_COLOUR('',#12376);
#12378=FILL_AREA_STYLE('',(#12377));
#12379=SURFACE_STYLE_FILL_AREA(#12378);
#12380=SURFACE_SIDE_STYLE('',(#12379));
#12381=SURFACE_STYLE_USAGE(.BOTH.,#12380);
#12382=PRESENTATION_STYLE_ASSIGNMENT((#12381));
ENDSEC;
END-ISO-10303-21;
